ISO-10303-21;
HEADER;
/* Generated by software containing ST-Developer
 * from STEP Tools, Inc. (www.steptools.com) 
 */

FILE_DESCRIPTION(
/* description */ ('Door-style hinge test fixture with detent'),
/* implementation_level */ '2;1');

FILE_NAME(
/* name */ 'Foot strip (1).step',
/* time_stamp */ '2026-10-28T03:24:57-07:00',
/* author */ (''),
/* organization */ (''),
/* preprocessor_version */ 'ST-DEVELOPER v20.2',
/* originating_system */ 'Autodesk Translation Framework v15.17.0.0',
/* authorisation */ '');

FILE_SCHEMA (('AUTOMOTIVE_DESIGN { 1 0 10303 214 3 1 1 }'));
ENDSEC;

DATA;
#10=MECHANICAL_DESIGN_GEOMETRIC_PRESENTATION_REPRESENTATION('',(#324),#9813);
#262=SHAPE_REPRESENTATION_RELATIONSHIP('SRR','None',#9939,#293);
#293=ADVANCED_BREP_SHAPE_REPRESENTATION('',(#364),#9782);
#324=STYLED_ITEM('',(#10169),#364);
#364=MANIFOLD_SOLID_BREP('Body1',#4755);
#512=PLANE('',#5167);
#513=PLANE('',#5168);
#514=PLANE('',#5169);
#515=PLANE('',#5170);
#516=PLANE('',#5171);
#517=PLANE('',#5172);
#679=FACE_OUTER_BOUND('',#972,.T.);
#680=FACE_OUTER_BOUND('',#973,.T.);
#681=FACE_OUTER_BOUND('',#974,.T.);
#682=FACE_OUTER_BOUND('',#975,.T.);
#683=FACE_OUTER_BOUND('',#976,.T.);
#684=FACE_OUTER_BOUND('',#977,.T.);
#972=EDGE_LOOP('',(#3279,#3280,#3281,#3282));
#973=EDGE_LOOP('',(#3283,#3284,#3285,#3286));
#974=EDGE_LOOP('',(#3287,#3288,#3289,#3290));
#975=EDGE_LOOP('',(#3291,#3292,#3293,#3294));
#976=EDGE_LOOP('',(#3295,#3296,#3297,#3298));
#977=EDGE_LOOP('',(#3299,#3300,#3301,#3302));
#1362=LINE('',#7381,#1682);
#1363=LINE('',#7383,#1683);
#1364=LINE('',#7385,#1684);
#1365=LINE('',#7386,#1685);
#1366=LINE('',#7389,#1686);
#1367=LINE('',#7391,#1687);
#1368=LINE('',#7392,#1688);
#1369=LINE('',#7395,#1689);
#1370=LINE('',#7397,#1690);
#1371=LINE('',#7398,#1691);
#1372=LINE('',#7400,#1692);
#1373=LINE('',#7401,#1693);
#1682=VECTOR('',#5839,1.);
#1683=VECTOR('',#5840,1.);
#1684=VECTOR('',#5841,1.);
#1685=VECTOR('',#5842,1.);
#1686=VECTOR('',#5845,1.);
#1687=VECTOR('',#5846,1.);
#1688=VECTOR('',#5847,1.);
#1689=VECTOR('',#5850,1.);
#1690=VECTOR('',#5851,1.);
#1691=VECTOR('',#5852,1.);
#1692=VECTOR('',#5855,1.);
#1693=VECTOR('',#5856,1.);
#2245=VERTEX_POINT('',#7379);
#2246=VERTEX_POINT('',#7380);
#2247=VERTEX_POINT('',#7382);
#2248=VERTEX_POINT('',#7384);
#2249=VERTEX_POINT('',#7388);
#2250=VERTEX_POINT('',#7390);
#2251=VERTEX_POINT('',#7394);
#2252=VERTEX_POINT('',#7396);
#2656=EDGE_CURVE('',#2245,#2246,#1362,.T.);
#2657=EDGE_CURVE('',#2246,#2247,#1363,.T.);
#2658=EDGE_CURVE('',#2248,#2247,#1364,.T.);
#2659=EDGE_CURVE('',#2245,#2248,#1365,.T.);
#2660=EDGE_CURVE('',#2249,#2245,#1366,.T.);
#2661=EDGE_CURVE('',#2250,#2248,#1367,.T.);
#2662=EDGE_CURVE('',#2249,#2250,#1368,.T.);
#2663=EDGE_CURVE('',#2251,#2249,#1369,.T.);
#2664=EDGE_CURVE('',#2252,#2250,#1370,.T.);
#2665=EDGE_CURVE('',#2251,#2252,#1371,.T.);
#2666=EDGE_CURVE('',#2246,#2251,#1372,.T.);
#2667=EDGE_CURVE('',#2247,#2252,#1373,.T.);
#3279=ORIENTED_EDGE('',*,*,#2656,.T.);
#3280=ORIENTED_EDGE('',*,*,#2657,.T.);
#3281=ORIENTED_EDGE('',*,*,#2658,.F.);
#3282=ORIENTED_EDGE('',*,*,#2659,.F.);
#3283=ORIENTED_EDGE('',*,*,#2660,.T.);
#3284=ORIENTED_EDGE('',*,*,#2659,.T.);
#3285=ORIENTED_EDGE('',*,*,#2661,.F.);
#3286=ORIENTED_EDGE('',*,*,#2662,.F.);
#3287=ORIENTED_EDGE('',*,*,#2663,.T.);
#3288=ORIENTED_EDGE('',*,*,#2662,.T.);
#3289=ORIENTED_EDGE('',*,*,#2664,.F.);
#3290=ORIENTED_EDGE('',*,*,#2665,.F.);
#3291=ORIENTED_EDGE('',*,*,#2666,.T.);
#3292=ORIENTED_EDGE('',*,*,#2665,.T.);
#3293=ORIENTED_EDGE('',*,*,#2667,.F.);
#3294=ORIENTED_EDGE('',*,*,#2657,.F.);
#3295=ORIENTED_EDGE('',*,*,#2667,.T.);
#3296=ORIENTED_EDGE('',*,*,#2664,.T.);
#3297=ORIENTED_EDGE('',*,*,#2661,.T.);
#3298=ORIENTED_EDGE('',*,*,#2658,.T.);
#3299=ORIENTED_EDGE('',*,*,#2666,.F.);
#3300=ORIENTED_EDGE('',*,*,#2656,.F.);
#3301=ORIENTED_EDGE('',*,*,#2660,.F.);
#3302=ORIENTED_EDGE('',*,*,#2663,.F.);
#4484=ADVANCED_FACE('',(#679),#512,.T.);
#4485=ADVANCED_FACE('',(#680),#513,.T.);
#4486=ADVANCED_FACE('',(#681),#514,.T.);
#4487=ADVANCED_FACE('',(#682),#515,.T.);
#4488=ADVANCED_FACE('',(#683),#516,.T.);
#4489=ADVANCED_FACE('',(#684),#517,.F.);
#4755=CLOSED_SHELL('',(#4484,#4485,#4486,#4487,#4488,#4489));
#5166=AXIS2_PLACEMENT_3D('',#7377,#5835,#5836);
#5167=AXIS2_PLACEMENT_3D('',#7378,#5837,#5838);
#5168=AXIS2_PLACEMENT_3D('',#7387,#5843,#5844);
#5169=AXIS2_PLACEMENT_3D('',#7393,#5848,#5849);
#5170=AXIS2_PLACEMENT_3D('',#7399,#5853,#5854);
#5171=AXIS2_PLACEMENT_3D('',#7402,#5857,#5858);
#5172=AXIS2_PLACEMENT_3D('',#7403,#5859,#5860);
#5835=DIRECTION('axis',(0.,0.,1.));
#5836=DIRECTION('refdir',(1.,0.,0.));
#5837=DIRECTION('center_axis',(0.,1.,0.));
#5838=DIRECTION('ref_axis',(-1.,0.,0.));
#5839=DIRECTION('',(-1.,0.,0.));
#5840=DIRECTION('',(0.,0.,1.));
#5841=DIRECTION('',(-1.,0.,0.));
#5842=DIRECTION('',(0.,0.,1.));
#5843=DIRECTION('center_axis',(1.,0.,0.));
#5844=DIRECTION('ref_axis',(0.,1.,0.));
#5845=DIRECTION('',(0.,1.,0.));
#5846=DIRECTION('',(0.,1.,0.));
#5847=DIRECTION('',(0.,0.,1.));
#5848=DIRECTION('center_axis',(0.,-1.,0.));
#5849=DIRECTION('ref_axis',(1.,0.,0.));
#5850=DIRECTION('',(1.,0.,0.));
#5851=DIRECTION('',(1.,0.,0.));
#5852=DIRECTION('',(0.,0.,1.));
#5853=DIRECTION('center_axis',(-1.,0.,0.));
#5854=DIRECTION('ref_axis',(0.,-1.,0.));
#5855=DIRECTION('',(0.,-1.,0.));
#5856=DIRECTION('',(0.,-1.,0.));
#5857=DIRECTION('center_axis',(0.,0.,1.));
#5858=DIRECTION('ref_axis',(1.,0.,0.));
#5859=DIRECTION('center_axis',(0.,0.,1.));
#5860=DIRECTION('ref_axis',(1.,0.,0.));
#7377=CARTESIAN_POINT('',(0.,0.,0.));
#7378=CARTESIAN_POINT('Origin',(13.5,13.5,-1.4));
#7379=CARTESIAN_POINT('',(13.5,13.5,-1.4));
#7380=CARTESIAN_POINT('',(11.5,13.5,-1.4));
#7381=CARTESIAN_POINT('',(13.5,13.5,-1.4));
#7382=CARTESIAN_POINT('',(11.5,13.5,-1.));
#7383=CARTESIAN_POINT('',(11.5,13.5,-1.4));
#7384=CARTESIAN_POINT('',(13.5,13.5,-1.));
#7385=CARTESIAN_POINT('',(13.5,13.5,-1.));
#7386=CARTESIAN_POINT('',(13.5,13.5,-1.4));
#7387=CARTESIAN_POINT('Origin',(13.5,-6.5,-1.4));
#7388=CARTESIAN_POINT('',(13.5,-6.5,-1.4));
#7389=CARTESIAN_POINT('',(13.5,-6.5,-1.4));
#7390=CARTESIAN_POINT('',(13.5,-6.5,-1.));
#7391=CARTESIAN_POINT('',(13.5,-6.5,-1.));
#7392=CARTESIAN_POINT('',(13.5,-6.5,-1.4));
#7393=CARTESIAN_POINT('Origin',(11.5,-6.5,-1.4));
#7394=CARTESIAN_POINT('',(11.5,-6.5,-1.4));
#7395=CARTESIAN_POINT('',(11.5,-6.5,-1.4));
#7396=CARTESIAN_POINT('',(11.5,-6.5,-1.));
#7397=CARTESIAN_POINT('',(11.5,-6.5,-1.));
#7398=CARTESIAN_POINT('',(11.5,-6.5,-1.4));
#7399=CARTESIAN_POINT('Origin',(11.5,13.5,-1.4));
#7400=CARTESIAN_POINT('',(11.5,13.5,-1.4));
#7401=CARTESIAN_POINT('',(11.5,13.5,-1.));
#7402=CARTESIAN_POINT('Origin',(12.5,3.5,-1.));
#7403=CARTESIAN_POINT('Origin',(12.5,3.5,-1.4));
#9746=UNCERTAINTY_MEASURE_WITH_UNIT(LENGTH_MEASURE(0.001),#9814,
'DISTANCE_ACCURACY_VALUE',
'Maximum model space distance between geometric entities at asserted c
onnectivities');
#9777=UNCERTAINTY_MEASURE_WITH_UNIT(LENGTH_MEASURE(0.001),#9814,
'DISTANCE_ACCURACY_VALUE',
'Maximum model space distance between geometric entities at asserted c
onnectivities');
#9782=(
GEOMETRIC_REPRESENTATION_CONTEXT(3)
GLOBAL_UNCERTAINTY_ASSIGNED_CONTEXT((#9746))
GLOBAL_UNIT_ASSIGNED_CONTEXT((#9814,#9816,#9817))
REPRESENTATION_CONTEXT('','3D')
);
#9813=(
GEOMETRIC_REPRESENTATION_CONTEXT(3)
GLOBAL_UNCERTAINTY_ASSIGNED_CONTEXT((#9777))
GLOBAL_UNIT_ASSIGNED_CONTEXT((#9814,#9816,#9817))
REPRESENTATION_CONTEXT('','3D')
);
#9814=(
LENGTH_UNIT()
NAMED_UNIT(*)
SI_UNIT(.CENTI.,.METRE.)
);
#9816=(
NAMED_UNIT(*)
PLANE_ANGLE_UNIT()
SI_UNIT($,.RADIAN.)
);
#9817=(
NAMED_UNIT(*)
SI_UNIT($,.STERADIAN.)
SOLID_ANGLE_UNIT()
);
#9822=SHAPE_DEFINITION_REPRESENTATION(#9857,#9939);
#9857=PRODUCT_DEFINITION_SHAPE('',$,#9975);
#9939=SHAPE_REPRESENTATION('',(#5166),#9782);
#9970=PRODUCT_DEFINITION_CONTEXT('part definition',#10077,'design');
#9975=PRODUCT_DEFINITION('Foot strip (1)','Foot strip (1)',#10010,#9970);
#10010=PRODUCT_DEFINITION_FORMATION('',$,#10083);
#10077=APPLICATION_CONTEXT(
'Core Data for Automotive Mechanical Design Process');
#10078=PRODUCT_CONTEXT('part definition',#10077,'mechanical');
#10083=PRODUCT('Foot strip (1)','Foot strip (1)','Foot strip (1)',(#10078));
#10163=COLOUR_RGB('Light Blue',0.38,0.62,0.78);
#10164=FILL_AREA_STYLE_COLOUR('',#10163);
#10165=FILL_AREA_STYLE('',(#10164));
#10166=SURFACE_STYLE_FILL_AREA(#10165);
#10167=SURFACE_SIDE_STYLE('',(#10166));
#10168=SURFACE_STYLE_USAGE(.BOTH.,#10167);
#10169=PRESENTATION_STYLE_ASSIGNMENT((#10168));
ENDSEC;
END-ISO-10303-21;
